ISO-10303-21;
HEADER;
/* Generated by software containing ST-Developer
 * from STEP Tools, Inc. (www.steptools.com) 
 */

FILE_DESCRIPTION(
/* description */ ('Shaft runout checking stand'),
/* implementation_level */ '2;1');

FILE_NAME(
/* name */ 'Inner race spacer (6).step',
/* time_stamp */ '2026-11-02T21:12:33-08:00',
/* author */ (''),
/* organization */ (''),
/* preprocessor_version */ 'ST-DEVELOPER v20.2',
/* originating_system */ 'Autodesk Translation Framework v15.17.0.0',
/* authorisation */ '');

FILE_SCHEMA (('AUTOMOTIVE_DESIGN { 1 0 10303 214 3 1 1 }'));
ENDSEC;

DATA;
#10=MECHANICAL_DESIGN_GEOMETRIC_PRESENTATION_REPRESENTATION('',(#495),#11748);
#409=SHAPE_REPRESENTATION_RELATIONSHIP('SRR','None',#11958,#452);
#452=ADVANCED_BREP_SHAPE_REPRESENTATION('',(#543),#11734);
#495=STYLED_ITEM('',(#12170),#543);
#543=MANIFOLD_SOLID_BREP('Body1',#6241);
#654=FACE_BOUND('',#1795,.T.);
#655=FACE_BOUND('',#1797,.T.);
#844=CIRCLE('',#7237,0.505);
#845=CIRCLE('',#7238,0.505);
#846=CIRCLE('',#7240,0.7);
#847=CIRCLE('',#7241,0.7);
#1015=CYLINDRICAL_SURFACE('',#7236,0.505);
#1016=CYLINDRICAL_SURFACE('',#7239,0.7);
#1332=FACE_OUTER_BOUND('',#1792,.T.);
#1333=FACE_OUTER_BOUND('',#1793,.T.);
#1334=FACE_OUTER_BOUND('',#1794,.T.);
#1335=FACE_OUTER_BOUND('',#1796,.T.);
#1792=EDGE_LOOP('',(#5326,#5327,#5328,#5329));
#1793=EDGE_LOOP('',(#5330,#5331,#5332,#5333));
#1794=EDGE_LOOP('',(#5334));
#1795=EDGE_LOOP('',(#5335));
#1796=EDGE_LOOP('',(#5336));
#1797=EDGE_LOOP('',(#5337));
#2325=LINE('',#10914,#2792);
#2326=LINE('',#10920,#2793);
#2792=VECTOR('',#8940,0.505);
#2793=VECTOR('',#8947,0.7);
#3228=VERTEX_POINT('',#10911);
#3229=VERTEX_POINT('',#10913);
#3230=VERTEX_POINT('',#10917);
#3231=VERTEX_POINT('',#10919);
#3949=EDGE_CURVE('',#3228,#3228,#844,.T.);
#3950=EDGE_CURVE('',#3228,#3229,#2325,.T.);
#3951=EDGE_CURVE('',#3229,#3229,#845,.T.);
#3952=EDGE_CURVE('',#3230,#3230,#846,.T.);
#3953=EDGE_CURVE('',#3230,#3231,#2326,.T.);
#3954=EDGE_CURVE('',#3231,#3231,#847,.T.);
#5326=ORIENTED_EDGE('',*,*,#3949,.F.);
#5327=ORIENTED_EDGE('',*,*,#3950,.T.);
#5328=ORIENTED_EDGE('',*,*,#3951,.T.);
#5329=ORIENTED_EDGE('',*,*,#3950,.F.);
#5330=ORIENTED_EDGE('',*,*,#3952,.F.);
#5331=ORIENTED_EDGE('',*,*,#3953,.T.);
#5332=ORIENTED_EDGE('',*,*,#3954,.T.);
#5333=ORIENTED_EDGE('',*,*,#3953,.F.);
#5334=ORIENTED_EDGE('',*,*,#3952,.T.);
#5335=ORIENTED_EDGE('',*,*,#3949,.T.);
#5336=ORIENTED_EDGE('',*,*,#3954,.F.);
#5337=ORIENTED_EDGE('',*,*,#3951,.F.);
#5809=PLANE('',#7242);
#5810=PLANE('',#7243);
#6132=ADVANCED_FACE('',(#1332),#1015,.F.);
#6133=ADVANCED_FACE('',(#1333),#1016,.T.);
#6134=ADVANCED_FACE('',(#1334,#654),#5809,.T.);
#6135=ADVANCED_FACE('',(#1335,#655),#5810,.F.);
#6241=CLOSED_SHELL('',(#6132,#6133,#6134,#6135));
#7235=AXIS2_PLACEMENT_3D('',#10909,#8934,#8935);
#7236=AXIS2_PLACEMENT_3D('',#10910,#8936,#8937);
#7237=AXIS2_PLACEMENT_3D('',#10912,#8938,#8939);
#7238=AXIS2_PLACEMENT_3D('',#10915,#8941,#8942);
#7239=AXIS2_PLACEMENT_3D('',#10916,#8943,#8944);
#7240=AXIS2_PLACEMENT_3D('',#10918,#8945,#8946);
#7241=AXIS2_PLACEMENT_3D('',#10921,#8948,#8949);
#7242=AXIS2_PLACEMENT_3D('',#10922,#8950,#8951);
#7243=AXIS2_PLACEMENT_3D('',#10923,#8952,#8953);
#8934=DIRECTION('axis',(0.,0.,1.));
#8935=DIRECTION('refdir',(1.,0.,0.));
#8936=DIRECTION('center_axis',(0.,1.,0.));
#8937=DIRECTION('ref_axis',(1.,0.,0.));
#8938=DIRECTION('center_axis',(0.,-1.,0.));
#8939=DIRECTION('ref_axis',(1.,0.,0.));
#8940=DIRECTION('',(0.,-1.,0.));
#8941=DIRECTION('center_axis',(0.,-1.,0.));
#8942=DIRECTION('ref_axis',(1.,0.,0.));
#8943=DIRECTION('center_axis',(0.,1.,0.));
#8944=DIRECTION('ref_axis',(1.,0.,0.));
#8945=DIRECTION('center_axis',(0.,1.,0.));
#8946=DIRECTION('ref_axis',(1.,0.,0.));
#8947=DIRECTION('',(0.,-1.,0.));
#8948=DIRECTION('center_axis',(0.,1.,0.));
#8949=DIRECTION('ref_axis',(1.,0.,0.));
#8950=DIRECTION('center_axis',(0.,1.,0.));
#8951=DIRECTION('ref_axis',(1.,0.,0.));
#8952=DIRECTION('center_axis',(0.,1.,0.));
#8953=DIRECTION('ref_axis',(1.,0.,0.));
#10909=CARTESIAN_POINT('',(0.,0.,0.));
#10910=CARTESIAN_POINT('Origin',(2.,9.2,5.));
#10911=CARTESIAN_POINT('',(1.495,9.55,5.));
#10912=CARTESIAN_POINT('Origin',(2.,9.55,5.));
#10913=CARTESIAN_POINT('',(1.495,9.2,5.));
#10914=CARTESIAN_POINT('',(1.495,9.2,5.));
#10915=CARTESIAN_POINT('Origin',(2.,9.2,5.));
#10916=CARTESIAN_POINT('Origin',(2.,9.2,5.));
#10917=CARTESIAN_POINT('',(1.3,9.55,5.));
#10918=CARTESIAN_POINT('Origin',(2.,9.55,5.));
#10919=CARTESIAN_POINT('',(1.3,9.2,5.));
#10920=CARTESIAN_POINT('',(1.3,9.2,5.));
#10921=CARTESIAN_POINT('Origin',(2.,9.2,5.));
#10922=CARTESIAN_POINT('Origin',(2.,9.55,5.));
#10923=CARTESIAN_POINT('Origin',(2.,9.2,5.));
#11685=UNCERTAINTY_MEASURE_WITH_UNIT(LENGTH_MEASURE(0.001),#11749,
'DISTANCE_ACCURACY_VALUE',
'Maximum model space distance between geometric entities at asserted c
onnectivities');
#11699=UNCERTAINTY_MEASURE_WITH_UNIT(LENGTH_MEASURE(0.001),#11749,
'DISTANCE_ACCURACY_VALUE',
'Maximum model space distance between geometric entities at asserted c
onnectivities');
#11734=(
GEOMETRIC_REPRESENTATION_CONTEXT(3)
GLOBAL_UNCERTAINTY_ASSIGNED_CONTEXT((#11685))
GLOBAL_UNIT_ASSIGNED_CONTEXT((#11749,#11751,#11752))
REPRESENTATION_CONTEXT('','3D')
);
#11748=(
GEOMETRIC_REPRESENTATION_CONTEXT(3)
GLOBAL_UNCERTAINTY_ASSIGNED_CONTEXT((#11699))
GLOBAL_UNIT_ASSIGNED_CONTEXT((#11749,#11751,#11752))
REPRESENTATION_CONTEXT('','3D')
);
#11749=(
LENGTH_UNIT()
NAMED_UNIT(*)
SI_UNIT(.CENTI.,.METRE.)
);
#11751=(
NAMED_UNIT(*)
PLANE_ANGLE_UNIT()
SI_UNIT($,.RADIAN.)
);
#11752=(
NAMED_UNIT(*)
SI_UNIT($,.STERADIAN.)
SOLID_ANGLE_UNIT()
);
#11787=SHAPE_DEFINITION_REPRESENTATION(#11835,#11958);
#11835=PRODUCT_DEFINITION_SHAPE('',$,#12007);
#11958=SHAPE_REPRESENTATION('',(#7235),#11734);
#11972=PRODUCT_DEFINITION_CONTEXT('part definition',#12118,'design');
#12007=PRODUCT_DEFINITION('Inner race spacer_6','Inner race spacer (6)',
#12055,#11972);
#12055=PRODUCT_DEFINITION_FORMATION('',$,#12154);
#12118=APPLICATION_CONTEXT(
'Core Data for Automotive Mechanical Design Process');
#12119=PRODUCT_CONTEXT('part definition',#12118,'mechanical');
#12154=PRODUCT('Inner race spacer_6','Inner race spacer (6)',
'Inner race spacer',(#12119));
#12170=PRESENTATION_STYLE_ASSIGNMENT((#12175));
#12175=SURFACE_STYLE_USAGE(.BOTH.,#12180);
#12180=SURFACE_SIDE_STYLE('',(#12185));
#12185=SURFACE_STYLE_FILL_AREA(#12190);
#12190=FILL_AREA_STYLE('CAD Library Painted - Steel gray',(#12195));
#12195=FILL_AREA_STYLE_COLOUR('CAD Library Painted - Steel gray',#12200);
#12200=COLOUR_RGB('CAD Library Painted - Steel gray',0.592156862745098,
0.631372549019608,0.67843137254902);
ENDSEC;
END-ISO-10303-21;
